ISO-10303-21;
HEADER;
/* Generated by software containing ST-Developer
 * from STEP Tools, Inc. (www.steptools.com) 
 */

FILE_DESCRIPTION(
/* description */ ('Worm-less right-angle friction wheel drive'),
/* implementation_level */ '2;1');

FILE_NAME(
/* name */ 'Bearing cap (1).step',
/* time_stamp */ '2026-10-28T03:22:36-07:00',
/* author */ (''),
/* organization */ (''),
/* preprocessor_version */ 'ST-DEVELOPER v20.2',
/* originating_system */ 'Autodesk Translation Framework v15.17.0.0',
/* authorisation */ '');

FILE_SCHEMA (('AUTOMOTIVE_DESIGN { 1 0 10303 214 3 1 1 }'));
ENDSEC;

DATA;
#10=MECHANICAL_DESIGN_GEOMETRIC_PRESENTATION_REPRESENTATION('',(#617),#17046);
#523=SHAPE_REPRESENTATION_RELATIONSHIP('SRR','None',#17266,#570);
#570=ADVANCED_BREP_SHAPE_REPRESENTATION('',(#671),#17002);
#617=STYLED_ITEM('',(#17591),#671);
#671=MANIFOLD_SOLID_BREP('Body1',#8172);
#776=FACE_BOUND('',#1822,.T.);
#777=FACE_BOUND('',#1826,.T.);
#778=FACE_BOUND('',#1827,.T.);
#779=FACE_BOUND('',#1828,.T.);
#780=FACE_BOUND('',#1829,.T.);
#781=FACE_BOUND('',#1830,.T.);
#782=FACE_BOUND('',#1832,.T.);
#783=FACE_BOUND('',#1833,.T.);
#784=FACE_BOUND('',#1834,.T.);
#785=FACE_BOUND('',#1835,.T.);
#786=FACE_BOUND('',#1836,.T.);
#997=PLANE('',#8919);
#998=PLANE('',#8926);
#999=PLANE('',#8927);
#1289=FACE_OUTER_BOUND('',#1816,.T.);
#1290=FACE_OUTER_BOUND('',#1817,.T.);
#1291=FACE_OUTER_BOUND('',#1818,.T.);
#1292=FACE_OUTER_BOUND('',#1819,.T.);
#1293=FACE_OUTER_BOUND('',#1820,.T.);
#1294=FACE_OUTER_BOUND('',#1821,.T.);
#1295=FACE_OUTER_BOUND('',#1823,.T.);
#1296=FACE_OUTER_BOUND('',#1824,.T.);
#1297=FACE_OUTER_BOUND('',#1825,.T.);
#1298=FACE_OUTER_BOUND('',#1831,.T.);
#1816=EDGE_LOOP('',(#5942,#5943,#5944,#5945));
#1817=EDGE_LOOP('',(#5946,#5947,#5948,#5949));
#1818=EDGE_LOOP('',(#5950,#5951,#5952,#5953));
#1819=EDGE_LOOP('',(#5954,#5955,#5956,#5957));
#1820=EDGE_LOOP('',(#5958,#5959,#5960,#5961));
#1821=EDGE_LOOP('',(#5962));
#1822=EDGE_LOOP('',(#5963));
#1823=EDGE_LOOP('',(#5964,#5965,#5966,#5967));
#1824=EDGE_LOOP('',(#5968,#5969,#5970,#5971));
#1825=EDGE_LOOP('',(#5972));
#1826=EDGE_LOOP('',(#5973));
#1827=EDGE_LOOP('',(#5974));
#1828=EDGE_LOOP('',(#5975));
#1829=EDGE_LOOP('',(#5976));
#1830=EDGE_LOOP('',(#5977));
#1831=EDGE_LOOP('',(#5978));
#1832=EDGE_LOOP('',(#5979));
#1833=EDGE_LOOP('',(#5980));
#1834=EDGE_LOOP('',(#5981));
#1835=EDGE_LOOP('',(#5982));
#1836=EDGE_LOOP('',(#5983));
#2509=LINE('',#12809,#3049);
#2510=LINE('',#12815,#3050);
#2511=LINE('',#12821,#3051);
#2512=LINE('',#12827,#3052);
#2513=LINE('',#12833,#3053);
#2514=LINE('',#12841,#3054);
#2515=LINE('',#12846,#3055);
#3049=VECTOR('',#10233,0.225);
#3050=VECTOR('',#10240,0.225);
#3051=VECTOR('',#10247,0.225);
#3052=VECTOR('',#10254,0.225);
#3053=VECTOR('',#10261,1.59);
#3054=VECTOR('',#10272,1.2);
#3055=VECTOR('',#10277,2.4);
#3529=CIRCLE('',#8905,0.225);
#3530=CIRCLE('',#8906,0.225);
#3531=CIRCLE('',#8908,0.225);
#3532=CIRCLE('',#8909,0.225);
#3533=CIRCLE('',#8911,0.225);
#3534=CIRCLE('',#8912,0.225);
#3535=CIRCLE('',#8914,0.225);
#3536=CIRCLE('',#8915,0.225);
#3537=CIRCLE('',#8917,1.59);
#3538=CIRCLE('',#8918,1.59);
#3539=CIRCLE('',#8920,1.2);
#3540=CIRCLE('',#8922,1.2);
#3541=CIRCLE('',#8924,2.4);
#3542=CIRCLE('',#8925,2.4);
#4005=VERTEX_POINT('',#12806);
#4006=VERTEX_POINT('',#12808);
#4007=VERTEX_POINT('',#12812);
#4008=VERTEX_POINT('',#12814);
#4009=VERTEX_POINT('',#12818);
#4010=VERTEX_POINT('',#12820);
#4011=VERTEX_POINT('',#12824);
#4012=VERTEX_POINT('',#12826);
#4013=VERTEX_POINT('',#12830);
#4014=VERTEX_POINT('',#12832);
#4015=VERTEX_POINT('',#12836);
#4016=VERTEX_POINT('',#12839);
#4017=VERTEX_POINT('',#12843);
#4018=VERTEX_POINT('',#12845);
#4740=EDGE_CURVE('',#4005,#4005,#3529,.T.);
#4741=EDGE_CURVE('',#4005,#4006,#2509,.T.);
#4742=EDGE_CURVE('',#4006,#4006,#3530,.T.);
#4743=EDGE_CURVE('',#4007,#4007,#3531,.T.);
#4744=EDGE_CURVE('',#4007,#4008,#2510,.T.);
#4745=EDGE_CURVE('',#4008,#4008,#3532,.T.);
#4746=EDGE_CURVE('',#4009,#4009,#3533,.T.);
#4747=EDGE_CURVE('',#4009,#4010,#2511,.T.);
#4748=EDGE_CURVE('',#4010,#4010,#3534,.T.);
#4749=EDGE_CURVE('',#4011,#4011,#3535,.T.);
#4750=EDGE_CURVE('',#4011,#4012,#2512,.T.);
#4751=EDGE_CURVE('',#4012,#4012,#3536,.T.);
#4752=EDGE_CURVE('',#4013,#4013,#3537,.T.);
#4753=EDGE_CURVE('',#4013,#4014,#2513,.T.);
#4754=EDGE_CURVE('',#4014,#4014,#3538,.T.);
#4755=EDGE_CURVE('',#4015,#4015,#3539,.T.);
#4756=EDGE_CURVE('',#4016,#4016,#3540,.T.);
#4757=EDGE_CURVE('',#4016,#4015,#2514,.T.);
#4758=EDGE_CURVE('',#4017,#4017,#3541,.T.);
#4759=EDGE_CURVE('',#4017,#4018,#2515,.T.);
#4760=EDGE_CURVE('',#4018,#4018,#3542,.T.);
#5942=ORIENTED_EDGE('',*,*,#4740,.F.);
#5943=ORIENTED_EDGE('',*,*,#4741,.T.);
#5944=ORIENTED_EDGE('',*,*,#4742,.F.);
#5945=ORIENTED_EDGE('',*,*,#4741,.F.);
#5946=ORIENTED_EDGE('',*,*,#4743,.F.);
#5947=ORIENTED_EDGE('',*,*,#4744,.T.);
#5948=ORIENTED_EDGE('',*,*,#4745,.F.);
#5949=ORIENTED_EDGE('',*,*,#4744,.F.);
#5950=ORIENTED_EDGE('',*,*,#4746,.F.);
#5951=ORIENTED_EDGE('',*,*,#4747,.T.);
#5952=ORIENTED_EDGE('',*,*,#4748,.F.);
#5953=ORIENTED_EDGE('',*,*,#4747,.F.);
#5954=ORIENTED_EDGE('',*,*,#4749,.F.);
#5955=ORIENTED_EDGE('',*,*,#4750,.T.);
#5956=ORIENTED_EDGE('',*,*,#4751,.F.);
#5957=ORIENTED_EDGE('',*,*,#4750,.F.);
#5958=ORIENTED_EDGE('',*,*,#4752,.F.);
#5959=ORIENTED_EDGE('',*,*,#4753,.T.);
#5960=ORIENTED_EDGE('',*,*,#4754,.T.);
#5961=ORIENTED_EDGE('',*,*,#4753,.F.);
#5962=ORIENTED_EDGE('',*,*,#4754,.F.);
#5963=ORIENTED_EDGE('',*,*,#4755,.F.);
#5964=ORIENTED_EDGE('',*,*,#4756,.F.);
#5965=ORIENTED_EDGE('',*,*,#4757,.T.);
#5966=ORIENTED_EDGE('',*,*,#4755,.T.);
#5967=ORIENTED_EDGE('',*,*,#4757,.F.);
#5968=ORIENTED_EDGE('',*,*,#4758,.F.);
#5969=ORIENTED_EDGE('',*,*,#4759,.T.);
#5970=ORIENTED_EDGE('',*,*,#4760,.T.);
#5971=ORIENTED_EDGE('',*,*,#4759,.F.);
#5972=ORIENTED_EDGE('',*,*,#4758,.T.);
#5973=ORIENTED_EDGE('',*,*,#4756,.T.);
#5974=ORIENTED_EDGE('',*,*,#4751,.T.);
#5975=ORIENTED_EDGE('',*,*,#4748,.T.);
#5976=ORIENTED_EDGE('',*,*,#4745,.T.);
#5977=ORIENTED_EDGE('',*,*,#4742,.T.);
#5978=ORIENTED_EDGE('',*,*,#4760,.F.);
#5979=ORIENTED_EDGE('',*,*,#4752,.T.);
#5980=ORIENTED_EDGE('',*,*,#4749,.T.);
#5981=ORIENTED_EDGE('',*,*,#4746,.T.);
#5982=ORIENTED_EDGE('',*,*,#4743,.T.);
#5983=ORIENTED_EDGE('',*,*,#4740,.T.);
#7566=CYLINDRICAL_SURFACE('',#8904,0.225);
#7567=CYLINDRICAL_SURFACE('',#8907,0.225);
#7568=CYLINDRICAL_SURFACE('',#8910,0.225);
#7569=CYLINDRICAL_SURFACE('',#8913,0.225);
#7570=CYLINDRICAL_SURFACE('',#8916,1.59);
#7571=CYLINDRICAL_SURFACE('',#8921,1.2);
#7572=CYLINDRICAL_SURFACE('',#8923,2.4);
#7781=ADVANCED_FACE('',(#1289),#7566,.F.);
#7782=ADVANCED_FACE('',(#1290),#7567,.F.);
#7783=ADVANCED_FACE('',(#1291),#7568,.F.);
#7784=ADVANCED_FACE('',(#1292),#7569,.F.);
#7785=ADVANCED_FACE('',(#1293),#7570,.T.);
#7786=ADVANCED_FACE('',(#1294,#776),#997,.F.);
#7787=ADVANCED_FACE('',(#1295),#7571,.F.);
#7788=ADVANCED_FACE('',(#1296),#7572,.T.);
#7789=ADVANCED_FACE('',(#1297,#777,#778,#779,#780,#781),#998,.T.);
#7790=ADVANCED_FACE('',(#1298,#782,#783,#784,#785,#786),#999,.F.);
#8172=CLOSED_SHELL('',(#7781,#7782,#7783,#7784,#7785,#7786,#7787,#7788,
#7789,#7790));
#8903=AXIS2_PLACEMENT_3D('',#12804,#10227,#10228);
#8904=AXIS2_PLACEMENT_3D('',#12805,#10229,#10230);
#8905=AXIS2_PLACEMENT_3D('',#12807,#10231,#10232);
#8906=AXIS2_PLACEMENT_3D('',#12810,#10234,#10235);
#8907=AXIS2_PLACEMENT_3D('',#12811,#10236,#10237);
#8908=AXIS2_PLACEMENT_3D('',#12813,#10238,#10239);
#8909=AXIS2_PLACEMENT_3D('',#12816,#10241,#10242);
#8910=AXIS2_PLACEMENT_3D('',#12817,#10243,#10244);
#8911=AXIS2_PLACEMENT_3D('',#12819,#10245,#10246);
#8912=AXIS2_PLACEMENT_3D('',#12822,#10248,#10249);
#8913=AXIS2_PLACEMENT_3D('',#12823,#10250,#10251);
#8914=AXIS2_PLACEMENT_3D('',#12825,#10252,#10253);
#8915=AXIS2_PLACEMENT_3D('',#12828,#10255,#10256);
#8916=AXIS2_PLACEMENT_3D('',#12829,#10257,#10258);
#8917=AXIS2_PLACEMENT_3D('',#12831,#10259,#10260);
#8918=AXIS2_PLACEMENT_3D('',#12834,#10262,#10263);
#8919=AXIS2_PLACEMENT_3D('',#12835,#10264,#10265);
#8920=AXIS2_PLACEMENT_3D('',#12837,#10266,#10267);
#8921=AXIS2_PLACEMENT_3D('',#12838,#10268,#10269);
#8922=AXIS2_PLACEMENT_3D('',#12840,#10270,#10271);
#8923=AXIS2_PLACEMENT_3D('',#12842,#10273,#10274);
#8924=AXIS2_PLACEMENT_3D('',#12844,#10275,#10276);
#8925=AXIS2_PLACEMENT_3D('',#12847,#10278,#10279);
#8926=AXIS2_PLACEMENT_3D('',#12848,#10280,#10281);
#8927=AXIS2_PLACEMENT_3D('',#12849,#10282,#10283);
#10227=DIRECTION('axis',(0.,0.,1.));
#10228=DIRECTION('refdir',(1.,0.,0.));
#10229=DIRECTION('center_axis',(0.,1.,0.));
#10230=DIRECTION('ref_axis',(1.,0.,0.));
#10231=DIRECTION('center_axis',(0.,1.,0.));
#10232=DIRECTION('ref_axis',(1.,0.,0.));
#10233=DIRECTION('',(0.,1.,0.));
#10234=DIRECTION('center_axis',(0.,-1.,0.));
#10235=DIRECTION('ref_axis',(1.,0.,0.));
#10236=DIRECTION('center_axis',(0.,1.,0.));
#10237=DIRECTION('ref_axis',(1.,0.,0.));
#10238=DIRECTION('center_axis',(0.,1.,0.));
#10239=DIRECTION('ref_axis',(1.,0.,0.));
#10240=DIRECTION('',(0.,1.,0.));
#10241=DIRECTION('center_axis',(0.,-1.,0.));
#10242=DIRECTION('ref_axis',(1.,0.,0.));
#10243=DIRECTION('center_axis',(0.,1.,0.));
#10244=DIRECTION('ref_axis',(1.,0.,0.));
#10245=DIRECTION('center_axis',(0.,1.,0.));
#10246=DIRECTION('ref_axis',(1.,0.,0.));
#10247=DIRECTION('',(0.,1.,0.));
#10248=DIRECTION('center_axis',(0.,-1.,0.));
#10249=DIRECTION('ref_axis',(1.,0.,0.));
#10250=DIRECTION('center_axis',(0.,1.,0.));
#10251=DIRECTION('ref_axis',(1.,0.,0.));
#10252=DIRECTION('center_axis',(0.,1.,0.));
#10253=DIRECTION('ref_axis',(1.,0.,0.));
#10254=DIRECTION('',(0.,1.,0.));
#10255=DIRECTION('center_axis',(0.,-1.,0.));
#10256=DIRECTION('ref_axis',(1.,0.,0.));
#10257=DIRECTION('center_axis',(0.,1.,0.));
#10258=DIRECTION('ref_axis',(1.,0.,0.));
#10259=DIRECTION('center_axis',(0.,1.,0.));
#10260=DIRECTION('ref_axis',(1.,0.,0.));
#10261=DIRECTION('',(0.,-1.,0.));
#10262=DIRECTION('center_axis',(0.,1.,0.));
#10263=DIRECTION('ref_axis',(1.,0.,0.));
#10264=DIRECTION('center_axis',(0.,1.,0.));
#10265=DIRECTION('ref_axis',(1.,0.,0.));
#10266=DIRECTION('center_axis',(0.,-1.,0.));
#10267=DIRECTION('ref_axis',(1.,0.,0.));
#10268=DIRECTION('center_axis',(0.,1.,0.));
#10269=DIRECTION('ref_axis',(1.,0.,0.));
#10270=DIRECTION('center_axis',(0.,-1.,0.));
#10271=DIRECTION('ref_axis',(1.,0.,0.));
#10272=DIRECTION('',(0.,-1.,0.));
#10273=DIRECTION('center_axis',(0.,1.,0.));
#10274=DIRECTION('ref_axis',(1.,0.,0.));
#10275=DIRECTION('center_axis',(0.,1.,0.));
#10276=DIRECTION('ref_axis',(1.,0.,0.));
#10277=DIRECTION('',(0.,-1.,0.));
#10278=DIRECTION('center_axis',(0.,1.,0.));
#10279=DIRECTION('ref_axis',(1.,0.,0.));
#10280=DIRECTION('center_axis',(0.,1.,0.));
#10281=DIRECTION('ref_axis',(1.,0.,0.));
#10282=DIRECTION('center_axis',(0.,1.,0.));
#10283=DIRECTION('ref_axis',(1.,0.,0.));
#12804=CARTESIAN_POINT('',(0.,0.,0.));
#12805=CARTESIAN_POINT('Origin',(-1.48492424049175,-6.3,5.51507575950825));
#12806=CARTESIAN_POINT('',(-1.70992424049175,-6.2,5.51507575950825));
#12807=CARTESIAN_POINT('Origin',(-1.48492424049175,-6.2,5.51507575950825));
#12808=CARTESIAN_POINT('',(-1.70992424049175,-6.,5.51507575950825));
#12809=CARTESIAN_POINT('',(-1.70992424049175,-6.3,5.51507575950825));
#12810=CARTESIAN_POINT('Origin',(-1.48492424049175,-6.,5.51507575950825));
#12811=CARTESIAN_POINT('Origin',(-1.48492424049175,-6.3,8.48492424049175));
#12812=CARTESIAN_POINT('',(-1.70992424049175,-6.2,8.48492424049175));
#12813=CARTESIAN_POINT('Origin',(-1.48492424049175,-6.2,8.48492424049175));
#12814=CARTESIAN_POINT('',(-1.70992424049175,-6.,8.48492424049175));
#12815=CARTESIAN_POINT('',(-1.70992424049175,-6.3,8.48492424049175));
#12816=CARTESIAN_POINT('Origin',(-1.48492424049175,-6.,8.48492424049175));
#12817=CARTESIAN_POINT('Origin',(1.48492424049175,-6.3,8.48492424049175));
#12818=CARTESIAN_POINT('',(1.25992424049175,-6.2,8.48492424049175));
#12819=CARTESIAN_POINT('Origin',(1.48492424049175,-6.2,8.48492424049175));
#12820=CARTESIAN_POINT('',(1.25992424049175,-6.,8.48492424049175));
#12821=CARTESIAN_POINT('',(1.25992424049175,-6.3,8.48492424049175));
#12822=CARTESIAN_POINT('Origin',(1.48492424049175,-6.,8.48492424049175));
#12823=CARTESIAN_POINT('Origin',(1.48492424049175,-6.3,5.51507575950825));
#12824=CARTESIAN_POINT('',(1.25992424049175,-6.2,5.51507575950825));
#12825=CARTESIAN_POINT('Origin',(1.48492424049175,-6.2,5.51507575950825));
#12826=CARTESIAN_POINT('',(1.25992424049175,-6.,5.51507575950825));
#12827=CARTESIAN_POINT('',(1.25992424049175,-6.3,5.51507575950825));
#12828=CARTESIAN_POINT('Origin',(1.48492424049175,-6.,5.51507575950825));
#12829=CARTESIAN_POINT('Origin',(0.,-6.5,7.));
#12830=CARTESIAN_POINT('',(-1.59,-6.2,7.));
#12831=CARTESIAN_POINT('Origin',(0.,-6.2,7.));
#12832=CARTESIAN_POINT('',(-1.59,-6.5,7.));
#12833=CARTESIAN_POINT('',(-1.59,-6.5,7.));
#12834=CARTESIAN_POINT('Origin',(0.,-6.5,7.));
#12835=CARTESIAN_POINT('Origin',(0.,-6.5,7.));
#12836=CARTESIAN_POINT('',(-1.2,-6.5,7.));
#12837=CARTESIAN_POINT('Origin',(0.,-6.5,7.));
#12838=CARTESIAN_POINT('Origin',(0.,-6.2,7.));
#12839=CARTESIAN_POINT('',(-1.2,-6.,7.));
#12840=CARTESIAN_POINT('Origin',(0.,-6.,7.));
#12841=CARTESIAN_POINT('',(-1.2,-6.2,7.));
#12842=CARTESIAN_POINT('Origin',(0.,-6.2,7.));
#12843=CARTESIAN_POINT('',(-2.4,-6.,7.));
#12844=CARTESIAN_POINT('Origin',(0.,-6.,7.));
#12845=CARTESIAN_POINT('',(-2.4,-6.2,7.));
#12846=CARTESIAN_POINT('',(-2.4,-6.2,7.));
#12847=CARTESIAN_POINT('Origin',(0.,-6.2,7.));
#12848=CARTESIAN_POINT('Origin',(0.,-6.,7.));
#12849=CARTESIAN_POINT('Origin',(0.,-6.2,7.));
#16949=UNCERTAINTY_MEASURE_WITH_UNIT(LENGTH_MEASURE(0.001),#17047,
'DISTANCE_ACCURACY_VALUE',
'Maximum model space distance between geometric entities at asserted c
onnectivities');
#16993=UNCERTAINTY_MEASURE_WITH_UNIT(LENGTH_MEASURE(0.001),#17047,
'DISTANCE_ACCURACY_VALUE',
'Maximum model space distance between geometric entities at asserted c
onnectivities');
#17002=(
GEOMETRIC_REPRESENTATION_CONTEXT(3)
GLOBAL_UNCERTAINTY_ASSIGNED_CONTEXT((#16949))
GLOBAL_UNIT_ASSIGNED_CONTEXT((#17047,#17049,#17050))
REPRESENTATION_CONTEXT('','3D')
);
#17046=(
GEOMETRIC_REPRESENTATION_CONTEXT(3)
GLOBAL_UNCERTAINTY_ASSIGNED_CONTEXT((#16993))
GLOBAL_UNIT_ASSIGNED_CONTEXT((#17047,#17049,#17050))
REPRESENTATION_CONTEXT('','3D')
);
#17047=(
LENGTH_UNIT()
NAMED_UNIT(*)
SI_UNIT(.CENTI.,.METRE.)
);
#17049=(
NAMED_UNIT(*)
PLANE_ANGLE_UNIT()
SI_UNIT($,.RADIAN.)
);
#17050=(
NAMED_UNIT(*)
SI_UNIT($,.STERADIAN.)
SOLID_ANGLE_UNIT()
);
#17059=SHAPE_DEFINITION_REPRESENTATION(#17111,#17266);
#17111=PRODUCT_DEFINITION_SHAPE('',$,#17319);
#17266=SHAPE_REPRESENTATION('',(#8903),#17002);
#17310=PRODUCT_DEFINITION_CONTEXT('part definition',#17468,'design');
#17319=PRODUCT_DEFINITION('Bearing cap (1)','Bearing cap (1)',#17371,#17310);
#17371=PRODUCT_DEFINITION_FORMATION('',$,#17478);
#17468=APPLICATION_CONTEXT(
'Core Data for Automotive Mechanical Design Process');
#17469=PRODUCT_CONTEXT('part definition',#17468,'mechanical');
#17478=PRODUCT('Bearing cap (1)','Bearing cap (1)','Bearing cap (1)',(#17469));
#17585=COLOUR_RGB('Grey',0.48,0.52,0.57);
#17586=FILL_AREA_STYLE_COLOUR('',#17585);
#17587=FILL_AREA_STYLE('',(#17586));
#17588=SURFACE_STYLE_FILL_AREA(#17587);
#17589=SURFACE_SIDE_STYLE('',(#17588));
#17590=SURFACE_STYLE_USAGE(.BOTH.,#17589);
#17591=PRESENTATION_STYLE_ASSIGNMENT((#17590));
ENDSEC;
END-ISO-10303-21;
